ISO-10303-21;
HEADER;
/* Generated by software containing ST-Developer
 * from STEP Tools, Inc. (www.steptools.com) 
 */

FILE_DESCRIPTION(
/* description */ (''),
/* implementation_level */ '2;1');

FILE_NAME(
/* name */ 'Bearing_03.step',
/* time_stamp */ '2026-10-19T01:30:23+06:00',
/* author */ (''),
/* organization */ (''),
/* preprocessor_version */ 'ST-DEVELOPER v20.2',
/* originating_system */ 'Autodesk Translation Framework v15.15.0.0',
/* authorisation */ '');

FILE_SCHEMA (('AUTOMOTIVE_DESIGN { 1 0 10303 214 3 1 1 }'));
ENDSEC;

DATA;
#10=MECHANICAL_DESIGN_GEOMETRIC_PRESENTATION_REPRESENTATION('',(#88),#10639);
#68=SHAPE_REPRESENTATION_RELATIONSHIP('SRR','None',#10678,#78);
#78=ADVANCED_BREP_SHAPE_REPRESENTATION('',(#98),#10630);
#88=STYLED_ITEM('',(#10790),#98);
#98=MANIFOLD_SOLID_BREP('Bearing_03',#5714);
#207=TOROIDAL_SURFACE('',#6175,4.3,0.3);
#208=TOROIDAL_SURFACE('',#6185,4.7,0.3);
#209=TOROIDAL_SURFACE('',#6192,4.3,0.3);
#210=TOROIDAL_SURFACE('',#6197,4.7,0.3);
#270=FACE_BOUND('',#953,.T.);
#271=FACE_BOUND('',#959,.T.);
#337=PLANE('',#6180);
#338=PLANE('',#6195);
#541=FACE_OUTER_BOUND('',#951,.T.);
#542=FACE_OUTER_BOUND('',#952,.T.);
#543=FACE_OUTER_BOUND('',#954,.T.);
#544=FACE_OUTER_BOUND('',#955,.T.);
#545=FACE_OUTER_BOUND('',#956,.T.);
#546=FACE_OUTER_BOUND('',#957,.T.);
#547=FACE_OUTER_BOUND('',#958,.T.);
#548=FACE_OUTER_BOUND('',#960,.T.);
#951=EDGE_LOOP('',(#4198,#4199,#4200,#4201,#4202));
#952=EDGE_LOOP('',(#4203));
#953=EDGE_LOOP('',(#4204));
#954=EDGE_LOOP('',(#4205,#4206,#4207,#4208,#4209,#4210));
#955=EDGE_LOOP('',(#4211,#4212,#4213,#4214,#4215));
#956=EDGE_LOOP('',(#4216,#4217,#4218,#4219,#4220,#4221));
#957=EDGE_LOOP('',(#4222,#4223,#4224,#4225,#4226));
#958=EDGE_LOOP('',(#4227));
#959=EDGE_LOOP('',(#4228));
#960=EDGE_LOOP('',(#4229,#4230,#4231,#4232,#4233));
#1347=LINE('',#9431,#1677);
#1348=LINE('',#9443,#1678);
#1677=VECTOR('',#7537,4.);
#1678=VECTOR('',#7552,5.);
#2028=CIRCLE('',#6176,4.3);
#2029=CIRCLE('',#6177,0.3);
#2030=CIRCLE('',#6178,4.);
#2031=CIRCLE('',#6179,4.);
#2032=CIRCLE('',#6181,4.7);
#2033=CIRCLE('',#6183,4.);
#2034=CIRCLE('',#6184,4.);
#2035=CIRCLE('',#6186,0.3);
#2036=CIRCLE('',#6187,5.);
#2037=CIRCLE('',#6188,5.);
#2038=CIRCLE('',#6190,5.);
#2039=CIRCLE('',#6191,5.);
#2040=CIRCLE('',#6193,4.3);
#2041=CIRCLE('',#6194,0.3);
#2042=CIRCLE('',#6196,4.7);
#2043=CIRCLE('',#6198,0.3);
#2486=VERTEX_POINT('',#9419);
#2487=VERTEX_POINT('',#9421);
#2488=VERTEX_POINT('',#9423);
#2489=VERTEX_POINT('',#9427);
#2490=VERTEX_POINT('',#9430);
#2491=VERTEX_POINT('',#9432);
#2492=VERTEX_POINT('',#9436);
#2493=VERTEX_POINT('',#9438);
#2494=VERTEX_POINT('',#9442);
#2495=VERTEX_POINT('',#9444);
#2496=VERTEX_POINT('',#9448);
#2497=VERTEX_POINT('',#9452);
#3075=EDGE_CURVE('',#2486,#2486,#2028,.T.);
#3076=EDGE_CURVE('',#2486,#2487,#2029,.T.);
#3077=EDGE_CURVE('',#2488,#2487,#2030,.T.);
#3078=EDGE_CURVE('',#2487,#2488,#2031,.T.);
#3079=EDGE_CURVE('',#2489,#2489,#2032,.T.);
#3080=EDGE_CURVE('',#2488,#2490,#1347,.T.);
#3081=EDGE_CURVE('',#2490,#2491,#2033,.T.);
#3082=EDGE_CURVE('',#2491,#2490,#2034,.T.);
#3083=EDGE_CURVE('',#2489,#2492,#2035,.T.);
#3084=EDGE_CURVE('',#2493,#2492,#2036,.T.);
#3085=EDGE_CURVE('',#2492,#2493,#2037,.T.);
#3086=EDGE_CURVE('',#2493,#2494,#1348,.T.);
#3087=EDGE_CURVE('',#2494,#2495,#2038,.T.);
#3088=EDGE_CURVE('',#2495,#2494,#2039,.T.);
#3089=EDGE_CURVE('',#2496,#2496,#2040,.T.);
#3090=EDGE_CURVE('',#2496,#2491,#2041,.T.);
#3091=EDGE_CURVE('',#2497,#2497,#2042,.T.);
#3092=EDGE_CURVE('',#2497,#2495,#2043,.T.);
#4198=ORIENTED_EDGE('',*,*,#3075,.F.);
#4199=ORIENTED_EDGE('',*,*,#3076,.T.);
#4200=ORIENTED_EDGE('',*,*,#3077,.F.);
#4201=ORIENTED_EDGE('',*,*,#3078,.F.);
#4202=ORIENTED_EDGE('',*,*,#3076,.F.);
#4203=ORIENTED_EDGE('',*,*,#3079,.T.);
#4204=ORIENTED_EDGE('',*,*,#3075,.T.);
#4205=ORIENTED_EDGE('',*,*,#3077,.T.);
#4206=ORIENTED_EDGE('',*,*,#3078,.T.);
#4207=ORIENTED_EDGE('',*,*,#3080,.T.);
#4208=ORIENTED_EDGE('',*,*,#3081,.T.);
#4209=ORIENTED_EDGE('',*,*,#3082,.T.);
#4210=ORIENTED_EDGE('',*,*,#3080,.F.);
#4211=ORIENTED_EDGE('',*,*,#3079,.F.);
#4212=ORIENTED_EDGE('',*,*,#3083,.T.);
#4213=ORIENTED_EDGE('',*,*,#3084,.F.);
#4214=ORIENTED_EDGE('',*,*,#3085,.F.);
#4215=ORIENTED_EDGE('',*,*,#3083,.F.);
#4216=ORIENTED_EDGE('',*,*,#3084,.T.);
#4217=ORIENTED_EDGE('',*,*,#3085,.T.);
#4218=ORIENTED_EDGE('',*,*,#3086,.T.);
#4219=ORIENTED_EDGE('',*,*,#3087,.T.);
#4220=ORIENTED_EDGE('',*,*,#3088,.T.);
#4221=ORIENTED_EDGE('',*,*,#3086,.F.);
#4222=ORIENTED_EDGE('',*,*,#3089,.F.);
#4223=ORIENTED_EDGE('',*,*,#3090,.T.);
#4224=ORIENTED_EDGE('',*,*,#3081,.F.);
#4225=ORIENTED_EDGE('',*,*,#3082,.F.);
#4226=ORIENTED_EDGE('',*,*,#3090,.F.);
#4227=ORIENTED_EDGE('',*,*,#3091,.T.);
#4228=ORIENTED_EDGE('',*,*,#3089,.T.);
#4229=ORIENTED_EDGE('',*,*,#3091,.F.);
#4230=ORIENTED_EDGE('',*,*,#3092,.T.);
#4231=ORIENTED_EDGE('',*,*,#3087,.F.);
#4232=ORIENTED_EDGE('',*,*,#3088,.F.);
#4233=ORIENTED_EDGE('',*,*,#3092,.F.);
#5223=CYLINDRICAL_SURFACE('',#6182,4.);
#5224=CYLINDRICAL_SURFACE('',#6189,5.);
#5484=ADVANCED_FACE('',(#541),#207,.T.);
#5485=ADVANCED_FACE('',(#542,#270),#337,.T.);
#5486=ADVANCED_FACE('',(#543),#5223,.F.);
#5487=ADVANCED_FACE('',(#544),#208,.T.);
#5488=ADVANCED_FACE('',(#545),#5224,.T.);
#5489=ADVANCED_FACE('',(#546),#209,.T.);
#5490=ADVANCED_FACE('',(#547,#271),#338,.F.);
#5491=ADVANCED_FACE('',(#548),#210,.T.);
#5714=CLOSED_SHELL('',(#5484,#5485,#5486,#5487,#5488,#5489,#5490,#5491));
#6174=AXIS2_PLACEMENT_3D('',#9417,#7519,#7520);
#6175=AXIS2_PLACEMENT_3D('',#9418,#7521,#7522);
#6176=AXIS2_PLACEMENT_3D('',#9420,#7523,#7524);
#6177=AXIS2_PLACEMENT_3D('',#9422,#7525,#7526);
#6178=AXIS2_PLACEMENT_3D('',#9424,#7527,#7528);
#6179=AXIS2_PLACEMENT_3D('',#9425,#7529,#7530);
#6180=AXIS2_PLACEMENT_3D('',#9426,#7531,#7532);
#6181=AXIS2_PLACEMENT_3D('',#9428,#7533,#7534);
#6182=AXIS2_PLACEMENT_3D('',#9429,#7535,#7536);
#6183=AXIS2_PLACEMENT_3D('',#9433,#7538,#7539);
#6184=AXIS2_PLACEMENT_3D('',#9434,#7540,#7541);
#6185=AXIS2_PLACEMENT_3D('',#9435,#7542,#7543);
#6186=AXIS2_PLACEMENT_3D('',#9437,#7544,#7545);
#6187=AXIS2_PLACEMENT_3D('',#9439,#7546,#7547);
#6188=AXIS2_PLACEMENT_3D('',#9440,#7548,#7549);
#6189=AXIS2_PLACEMENT_3D('',#9441,#7550,#7551);
#6190=AXIS2_PLACEMENT_3D('',#9445,#7553,#7554);
#6191=AXIS2_PLACEMENT_3D('',#9446,#7555,#7556);
#6192=AXIS2_PLACEMENT_3D('',#9447,#7557,#7558);
#6193=AXIS2_PLACEMENT_3D('',#9449,#7559,#7560);
#6194=AXIS2_PLACEMENT_3D('',#9450,#7561,#7562);
#6195=AXIS2_PLACEMENT_3D('',#9451,#7563,#7564);
#6196=AXIS2_PLACEMENT_3D('',#9453,#7565,#7566);
#6197=AXIS2_PLACEMENT_3D('',#9454,#7567,#7568);
#6198=AXIS2_PLACEMENT_3D('',#9455,#7569,#7570);
#7519=DIRECTION('axis',(0.,0.,1.));
#7520=DIRECTION('refdir',(1.,0.,0.));
#7521=DIRECTION('center_axis',(-1.,0.,0.));
#7522=DIRECTION('ref_axis',(0.,0.,1.));
#7523=DIRECTION('center_axis',(-1.,0.,0.));
#7524=DIRECTION('ref_axis',(0.,1.,0.));
#7525=DIRECTION('center_axis',(0.,-1.,0.));
#7526=DIRECTION('ref_axis',(0.,0.,-1.));
#7527=DIRECTION('center_axis',(1.,0.,0.));
#7528=DIRECTION('ref_axis',(0.,1.,0.));
#7529=DIRECTION('center_axis',(1.,0.,0.));
#7530=DIRECTION('ref_axis',(0.,1.,0.));
#7531=DIRECTION('center_axis',(1.,0.,0.));
#7532=DIRECTION('ref_axis',(0.,1.,0.));
#7533=DIRECTION('center_axis',(1.,0.,0.));
#7534=DIRECTION('ref_axis',(0.,1.,0.));
#7535=DIRECTION('center_axis',(-1.,0.,0.));
#7536=DIRECTION('ref_axis',(0.,1.,0.));
#7537=DIRECTION('',(-1.,0.,0.));
#7538=DIRECTION('center_axis',(-1.,0.,0.));
#7539=DIRECTION('ref_axis',(0.,1.,0.));
#7540=DIRECTION('center_axis',(-1.,0.,0.));
#7541=DIRECTION('ref_axis',(0.,1.,0.));
#7542=DIRECTION('center_axis',(1.,0.,0.));
#7543=DIRECTION('ref_axis',(0.,0.,-1.));
#7544=DIRECTION('center_axis',(0.,-1.,0.));
#7545=DIRECTION('ref_axis',(0.,0.,1.));
#7546=DIRECTION('center_axis',(-1.,0.,0.));
#7547=DIRECTION('ref_axis',(0.,1.,0.));
#7548=DIRECTION('center_axis',(-1.,0.,0.));
#7549=DIRECTION('ref_axis',(0.,1.,0.));
#7550=DIRECTION('center_axis',(-1.,0.,0.));
#7551=DIRECTION('ref_axis',(0.,1.,0.));
#7552=DIRECTION('',(-1.,0.,0.));
#7553=DIRECTION('center_axis',(1.,0.,0.));
#7554=DIRECTION('ref_axis',(0.,1.,0.));
#7555=DIRECTION('center_axis',(1.,0.,0.));
#7556=DIRECTION('ref_axis',(0.,1.,0.));
#7557=DIRECTION('center_axis',(1.,0.,0.));
#7558=DIRECTION('ref_axis',(0.,0.,-1.));
#7559=DIRECTION('center_axis',(1.,0.,0.));
#7560=DIRECTION('ref_axis',(0.,1.,0.));
#7561=DIRECTION('center_axis',(0.,-1.,0.));
#7562=DIRECTION('ref_axis',(0.,0.,1.));
#7563=DIRECTION('center_axis',(1.,0.,0.));
#7564=DIRECTION('ref_axis',(0.,1.,0.));
#7565=DIRECTION('center_axis',(-1.,0.,0.));
#7566=DIRECTION('ref_axis',(0.,1.,0.));
#7567=DIRECTION('center_axis',(-1.,0.,0.));
#7568=DIRECTION('ref_axis',(0.,0.,1.));
#7569=DIRECTION('center_axis',(0.,-1.,0.));
#7570=DIRECTION('ref_axis',(0.,0.,-1.));
#9417=CARTESIAN_POINT('',(0.,0.,0.));
#9418=CARTESIAN_POINT('Origin',(-13.3,-21.9999999999999,-1.92966607280848));
#9419=CARTESIAN_POINT('',(-13.,-21.9999999999999,-6.22966607280848));
#9420=CARTESIAN_POINT('Origin',(-13.,-21.9999999999999,-1.92966607280848));
#9421=CARTESIAN_POINT('',(-13.3,-21.9999999999999,-5.92966607280848));
#9422=CARTESIAN_POINT('Origin',(-13.3,-21.9999999999999,-6.22966607280848));
#9423=CARTESIAN_POINT('',(-13.3,-25.9999999999999,-1.92966607280848));
#9424=CARTESIAN_POINT('Origin',(-13.3,-21.9999999999999,-1.92966607280848));
#9425=CARTESIAN_POINT('Origin',(-13.3,-21.9999999999999,-1.92966607280848));
#9426=CARTESIAN_POINT('Origin',(-13.,-21.9999999999999,-1.92966607280848));
#9427=CARTESIAN_POINT('',(-13.,-21.9999999999999,2.77033392719152));
#9428=CARTESIAN_POINT('Origin',(-13.,-21.9999999999999,-1.92966607280848));
#9429=CARTESIAN_POINT('Origin',(-29.,-21.9999999999999,-1.92966607280848));
#9430=CARTESIAN_POINT('',(-28.7,-25.9999999999999,-1.92966607280848));
#9431=CARTESIAN_POINT('',(-29.,-25.9999999999999,-1.92966607280848));
#9432=CARTESIAN_POINT('',(-28.7,-21.9999999999999,2.07033392719152));
#9433=CARTESIAN_POINT('Origin',(-28.7,-21.9999999999999,-1.92966607280848));
#9434=CARTESIAN_POINT('Origin',(-28.7,-21.9999999999999,-1.92966607280848));
#9435=CARTESIAN_POINT('Origin',(-13.3,-21.9999999999999,-1.92966607280848));
#9436=CARTESIAN_POINT('',(-13.3,-21.9999999999999,3.07033392719152));
#9437=CARTESIAN_POINT('Origin',(-13.3,-21.9999999999999,2.77033392719152));
#9438=CARTESIAN_POINT('',(-13.3,-26.9999999999999,-1.92966607280848));
#9439=CARTESIAN_POINT('Origin',(-13.3,-21.9999999999999,-1.92966607280848));
#9440=CARTESIAN_POINT('Origin',(-13.3,-21.9999999999999,-1.92966607280848));
#9441=CARTESIAN_POINT('Origin',(-29.,-21.9999999999999,-1.92966607280848));
#9442=CARTESIAN_POINT('',(-28.7,-26.9999999999999,-1.92966607280848));
#9443=CARTESIAN_POINT('',(-29.,-26.9999999999999,-1.92966607280848));
#9444=CARTESIAN_POINT('',(-28.7,-21.9999999999999,-6.92966607280848));
#9445=CARTESIAN_POINT('Origin',(-28.7,-21.9999999999999,-1.92966607280848));
#9446=CARTESIAN_POINT('Origin',(-28.7,-21.9999999999999,-1.92966607280848));
#9447=CARTESIAN_POINT('Origin',(-28.7,-21.9999999999999,-1.92966607280848));
#9448=CARTESIAN_POINT('',(-29.,-21.9999999999999,2.37033392719152));
#9449=CARTESIAN_POINT('Origin',(-29.,-21.9999999999999,-1.92966607280848));
#9450=CARTESIAN_POINT('Origin',(-28.7,-21.9999999999999,2.37033392719152));
#9451=CARTESIAN_POINT('Origin',(-29.,-21.9999999999999,-1.92966607280848));
#9452=CARTESIAN_POINT('',(-29.,-21.9999999999999,-6.62966607280848));
#9453=CARTESIAN_POINT('Origin',(-29.,-21.9999999999999,-1.92966607280848));
#9454=CARTESIAN_POINT('Origin',(-28.7,-21.9999999999999,-1.92966607280848));
#9455=CARTESIAN_POINT('Origin',(-28.7,-21.9999999999999,-6.62966607280848));
#10618=UNCERTAINTY_MEASURE_WITH_UNIT(LENGTH_MEASURE(0.01),#10640,
'DISTANCE_ACCURACY_VALUE',
'Maximum model space distance between geometric entities at asserted c
onnectivities');
#10627=UNCERTAINTY_MEASURE_WITH_UNIT(LENGTH_MEASURE(0.01),#10640,
'DISTANCE_ACCURACY_VALUE',
'Maximum model space distance between geometric entities at asserted c
onnectivities');
#10630=(
GEOMETRIC_REPRESENTATION_CONTEXT(3)
GLOBAL_UNCERTAINTY_ASSIGNED_CONTEXT((#10618))
GLOBAL_UNIT_ASSIGNED_CONTEXT((#10640,#10642,#10643))
REPRESENTATION_CONTEXT('','3D')
);
#10639=(
GEOMETRIC_REPRESENTATION_CONTEXT(3)
GLOBAL_UNCERTAINTY_ASSIGNED_CONTEXT((#10627))
GLOBAL_UNIT_ASSIGNED_CONTEXT((#10640,#10642,#10643))
REPRESENTATION_CONTEXT('','3D')
);
#10640=(
LENGTH_UNIT()
NAMED_UNIT(*)
SI_UNIT(.MILLI.,.METRE.)
);
#10642=(
NAMED_UNIT(*)
PLANE_ANGLE_UNIT()
SI_UNIT($,.RADIAN.)
);
#10643=(
NAMED_UNIT(*)
SI_UNIT($,.STERADIAN.)
SOLID_ANGLE_UNIT()
);
#10646=SHAPE_DEFINITION_REPRESENTATION(#10657,#10678);
#10657=PRODUCT_DEFINITION_SHAPE('',$,#10690);
#10678=SHAPE_REPRESENTATION('',(#6174),#10630);
#10687=PRODUCT_DEFINITION_CONTEXT('part definition',#10722,'design');
#10690=PRODUCT_DEFINITION('Bearing_03','Bearing_03',#10701,#10687);
#10701=PRODUCT_DEFINITION_FORMATION('',$,#10726);
#10722=APPLICATION_CONTEXT(
'Core Data for Automotive Mechanical Design Process');
#10723=PRODUCT_CONTEXT('part definition',#10722,'mechanical');
#10726=PRODUCT('Bearing_03','Bearing_03',$,(#10723));
#10784=COLOUR_RGB('Grey',0.48,0.52,0.57);
#10785=FILL_AREA_STYLE_COLOUR('',#10784);
#10786=FILL_AREA_STYLE('',(#10785));
#10787=SURFACE_STYLE_FILL_AREA(#10786);
#10788=SURFACE_SIDE_STYLE('',(#10787));
#10789=SURFACE_STYLE_USAGE(.BOTH.,#10788);
#10790=PRESENTATION_STYLE_ASSIGNMENT((#10789));
ENDSEC;
END-ISO-10303-21;
